ISO-10303-21;
HEADER;
/* Generated by software containing ST-Developer
 * from STEP Tools, Inc. (www.steptools.com) 
 */
/* OPTION: using custom renumber hook */

FILE_DESCRIPTION(
/* description */ ('STEP AP242 Edition 2', 'CAx-IF Rec.Pracs.---Representation and Presentation of Product Manufa
cturing Information (PMI)---4.0---2014-10-13', 'CAx-IF Rec.Pracs.---3D Tessellated Geometry---0.4---2014-09-14', '2;1', 'CAx-IF Rec.Pracs.---User Defined Attributes---1.5---2016-08-15'),
/* implementation_level */ '2;1');

FILE_NAME(
/* name */ 'Slotted cheese head screw M2.5x0.45 x 10.step',
/* time_stamp */ '2026-10-09T13:59:33Z',
/* author */ (''),
/* organization */ (''),
/* preprocessor_version */ 'ST-DEVELOPER v20',
/* originating_system */ 'ONSHAPE BY PTC INC, 1.221',
/* authorisation */ '  ');

FILE_SCHEMA (('AP242_MANAGED_MODEL_BASED_3D_ENGINEERING_MIM_LF { 1 0 10303 442 3 1 4 }'));
ENDSEC;

DATA;
#10=CONICAL_SURFACE('',#5743,0.00209252040565334,0.0872664625997158);
#11=CONICAL_SURFACE('',#5755,0.00100643035625,0.785398163397448);
#17=TOROIDAL_SURFACE('',#5734,0.0020008872882516,0.0001);
#18=TOROIDAL_SURFACE('',#5750,0.00135,0.0001);
#19=TOROIDAL_SURFACE('',#5751,0.0020008872882516,0.0001);
#35=LINE('',#8458,#319);
#36=LINE('',#8486,#320);
#37=LINE('',#8529,#321);
#38=LINE('',#8530,#322);
#319=VECTOR('',#6563,1.);
#320=VECTOR('',#6584,1.);
#321=VECTOR('',#6605,1.);
#322=VECTOR('',#6606,1.);
#672=SHAPE_REPRESENTATION_RELATIONSHIP('','',#5690,#686);
#686=ADVANCED_BREP_SHAPE_REPRESENTATION('',(#5659),#10144);
#703=PLANE('',#5732);
#704=PLANE('',#5740);
#705=PLANE('',#5742);
#706=PLANE('',#5748);
#707=PLANE('',#5752);
#708=PLANE('',#5753);
#709=PLANE('',#5754);
#792=B_SPLINE_CURVE_WITH_KNOTS('',3,(#8466,#8467,#8468,#8469),
 .UNSPECIFIED.,.F.,.F.,(4,4),(0.000582701576065907,0.000731093758582388),
 .UNSPECIFIED.);
#793=B_SPLINE_CURVE_WITH_KNOTS('',3,(#8473,#8474,#8475,#8476),
 .UNSPECIFIED.,.F.,.F.,(4,4),(0.000110312006623771,0.000258881093106313),
 .UNSPECIFIED.);
#794=B_SPLINE_CURVE_WITH_KNOTS('',3,(#8491,#8492,#8493,#8494),
 .UNSPECIFIED.,.F.,.F.,(4,4),(0.00363875425759936,0.00424984212477264),
 .UNSPECIFIED.);
#795=B_SPLINE_CURVE_WITH_KNOTS('',3,(#8498,#8499,#8500,#8501),
 .UNSPECIFIED.,.F.,.F.,(4,4),(0.00363875425759936,0.00424984212477264),
 .UNSPECIFIED.);
#796=B_SPLINE_CURVE_WITH_KNOTS('',3,(#8502,#8503,#8504,#8505),
 .UNSPECIFIED.,.F.,.F.,(4,4),(0.00356470722087229,0.00417579509082418),
 .UNSPECIFIED.);
#797=B_SPLINE_CURVE_WITH_KNOTS('',3,(#8509,#8510,#8511,#8512),
 .UNSPECIFIED.,.F.,.F.,(4,4),(0.00356470722087229,0.00417579509082374),
 .UNSPECIFIED.);
#798=B_SPLINE_CURVE_WITH_KNOTS('',3,(#8520,#8521,#8522,#8523),
 .UNSPECIFIED.,.F.,.F.,(4,4),(0.000582701576065907,0.000731093758582387),
 .UNSPECIFIED.);
#799=B_SPLINE_CURVE_WITH_KNOTS('',3,(#8524,#8525,#8526,#8527),
 .UNSPECIFIED.,.F.,.F.,(4,4),(0.000110312006623771,0.000258881093106891),
 .UNSPECIFIED.);
#846=ORIENTED_EDGE('',*,*,#2360,.F.);
#847=ORIENTED_EDGE('',*,*,#2361,.T.);
#848=ORIENTED_EDGE('',*,*,#2362,.F.);
#849=ORIENTED_EDGE('',*,*,#2363,.T.);
#850=ORIENTED_EDGE('',*,*,#2364,.F.);
#851=ORIENTED_EDGE('',*,*,#2365,.T.);
#852=ORIENTED_EDGE('',*,*,#2366,.T.);
#853=ORIENTED_EDGE('',*,*,#2367,.T.);
#854=ORIENTED_EDGE('',*,*,#2368,.T.);
#855=ORIENTED_EDGE('',*,*,#2364,.T.);
#856=ORIENTED_EDGE('',*,*,#2369,.T.);
#857=ORIENTED_EDGE('',*,*,#2370,.T.);
#858=ORIENTED_EDGE('',*,*,#2371,.T.);
#859=ORIENTED_EDGE('',*,*,#2372,.F.);
#860=ORIENTED_EDGE('',*,*,#2373,.F.);
#861=ORIENTED_EDGE('',*,*,#2362,.T.);
#862=ORIENTED_EDGE('',*,*,#2374,.F.);
#863=ORIENTED_EDGE('',*,*,#2375,.F.);
#864=ORIENTED_EDGE('',*,*,#2376,.T.);
#865=ORIENTED_EDGE('',*,*,#2377,.F.);
#866=ORIENTED_EDGE('',*,*,#2378,.F.);
#867=ORIENTED_EDGE('',*,*,#2377,.T.);
#868=ORIENTED_EDGE('',*,*,#2378,.T.);
#869=ORIENTED_EDGE('',*,*,#2367,.F.);
#870=ORIENTED_EDGE('',*,*,#2379,.F.);
#871=ORIENTED_EDGE('',*,*,#2370,.F.);
#872=ORIENTED_EDGE('',*,*,#2380,.F.);
#873=ORIENTED_EDGE('',*,*,#2361,.F.);
#874=ORIENTED_EDGE('',*,*,#2372,.T.);
#875=ORIENTED_EDGE('',*,*,#2381,.T.);
#876=ORIENTED_EDGE('',*,*,#2375,.T.);
#877=ORIENTED_EDGE('',*,*,#2382,.F.);
#878=ORIENTED_EDGE('',*,*,#2379,.T.);
#879=ORIENTED_EDGE('',*,*,#2360,.T.);
#880=ORIENTED_EDGE('',*,*,#2380,.T.);
#881=ORIENTED_EDGE('',*,*,#2376,.F.);
#882=ORIENTED_EDGE('',*,*,#2381,.F.);
#883=ORIENTED_EDGE('',*,*,#2371,.F.);
#884=ORIENTED_EDGE('',*,*,#2373,.T.);
#885=ORIENTED_EDGE('',*,*,#2382,.T.);
#886=ORIENTED_EDGE('',*,*,#2374,.T.);
#887=ORIENTED_EDGE('',*,*,#2365,.F.);
#888=ORIENTED_EDGE('',*,*,#2369,.F.);
#889=ORIENTED_EDGE('',*,*,#2363,.F.);
#890=ORIENTED_EDGE('',*,*,#2366,.F.);
#891=ORIENTED_EDGE('',*,*,#2368,.F.);
#2360=EDGE_CURVE('',#3125,#3126,#35,.T.);
#2361=EDGE_CURVE('',#3125,#3126,#3664,.F.);
#2362=EDGE_CURVE('',#3127,#3128,#3665,.F.);
#2363=EDGE_CURVE('',#3127,#3129,#792,.T.);
#2364=EDGE_CURVE('',#3130,#3129,#3666,.F.);
#2365=EDGE_CURVE('',#3130,#3128,#793,.T.);
#2366=EDGE_CURVE('',#3131,#3131,#3667,.T.);
#2367=EDGE_CURVE('',#3132,#3132,#3668,.T.);
#2368=EDGE_CURVE('',#3133,#3133,#3669,.F.);
#2369=EDGE_CURVE('',#3129,#3130,#36,.T.);
#2370=EDGE_CURVE('',#3134,#3135,#3670,.F.);
#2371=EDGE_CURVE('',#3135,#3136,#794,.T.);
#2372=EDGE_CURVE('',#3137,#3136,#3671,.T.);
#2373=EDGE_CURVE('',#3127,#3137,#795,.T.);
#2374=EDGE_CURVE('',#3138,#3128,#796,.T.);
#2375=EDGE_CURVE('',#3139,#3138,#3672,.T.);
#2376=EDGE_CURVE('',#3139,#3134,#797,.T.);
#2377=EDGE_CURVE('',#3140,#3140,#3673,.T.);
#2378=EDGE_CURVE('',#3141,#3141,#3674,.T.);
#2379=EDGE_CURVE('',#3135,#3125,#798,.T.);
#2380=EDGE_CURVE('',#3126,#3134,#799,.T.);
#2381=EDGE_CURVE('',#3136,#3139,#37,.T.);
#2382=EDGE_CURVE('',#3137,#3138,#38,.T.);
#3125=VERTEX_POINT('',#8459);
#3126=VERTEX_POINT('',#8460);
#3127=VERTEX_POINT('',#8464);
#3128=VERTEX_POINT('',#8465);
#3129=VERTEX_POINT('',#8470);
#3130=VERTEX_POINT('',#8472);
#3131=VERTEX_POINT('',#8479);
#3132=VERTEX_POINT('',#8481);
#3133=VERTEX_POINT('',#8484);
#3134=VERTEX_POINT('',#8489);
#3135=VERTEX_POINT('',#8490);
#3136=VERTEX_POINT('',#8495);
#3137=VERTEX_POINT('',#8497);
#3138=VERTEX_POINT('',#8506);
#3139=VERTEX_POINT('',#8508);
#3140=VERTEX_POINT('',#8514);
#3141=VERTEX_POINT('',#8517);
#3664=CIRCLE('',#5733,0.0020008872882516);
#3665=CIRCLE('',#5735,0.00210050675806077);
#3666=CIRCLE('',#5736,0.0020008872882516);
#3667=CIRCLE('',#5738,0.00125);
#3668=CIRCLE('',#5739,0.00125);
#3669=CIRCLE('',#5741,0.00100643035625);
#3670=CIRCLE('',#5744,0.00210050675806077);
#3671=CIRCLE('',#5745,0.00215376247012148);
#3672=CIRCLE('',#5746,0.00215376247012148);
#3673=CIRCLE('',#5747,0.00225);
#3674=CIRCLE('',#5749,0.00135);
#4139=EDGE_LOOP('',(#846,#847));
#4140=EDGE_LOOP('',(#848,#849,#850,#851));
#4141=EDGE_LOOP('',(#852));
#4142=EDGE_LOOP('',(#853));
#4143=EDGE_LOOP('',(#854));
#4144=EDGE_LOOP('',(#855,#856));
#4145=EDGE_LOOP('',(#857,#858,#859,#860,#861,#862,#863,#864));
#4146=EDGE_LOOP('',(#865));
#4147=EDGE_LOOP('',(#866));
#4148=EDGE_LOOP('',(#867));
#4149=EDGE_LOOP('',(#868));
#4150=EDGE_LOOP('',(#869));
#4151=EDGE_LOOP('',(#870,#871,#872,#873));
#4152=EDGE_LOOP('',(#874,#875,#876,#877));
#4153=EDGE_LOOP('',(#878,#879,#880,#881,#882,#883));
#4154=EDGE_LOOP('',(#884,#885,#886,#887,#888,#889));
#4155=EDGE_LOOP('',(#890));
#4156=EDGE_LOOP('',(#891));
#4587=FACE_BOUND('',#4139,.T.);
#4588=FACE_BOUND('',#4140,.T.);
#4589=FACE_BOUND('',#4141,.T.);
#4590=FACE_BOUND('',#4142,.T.);
#4591=FACE_BOUND('',#4143,.T.);
#4592=FACE_BOUND('',#4144,.T.);
#4593=FACE_BOUND('',#4145,.T.);
#4594=FACE_BOUND('',#4146,.T.);
#4595=FACE_BOUND('',#4147,.T.);
#4596=FACE_BOUND('',#4148,.T.);
#4597=FACE_BOUND('',#4149,.T.);
#4598=FACE_BOUND('',#4150,.T.);
#4599=FACE_BOUND('',#4151,.T.);
#4600=FACE_BOUND('',#4152,.T.);
#4601=FACE_BOUND('',#4153,.T.);
#4602=FACE_BOUND('',#4154,.T.);
#4603=FACE_BOUND('',#4155,.T.);
#4604=FACE_BOUND('',#4156,.T.);
#5011=CYLINDRICAL_SURFACE('',#5737,0.00125);
#5225=ADVANCED_FACE('',(#4587),#703,.F.);
#5226=ADVANCED_FACE('',(#4588),#17,.T.);
#5227=ADVANCED_FACE('',(#4589,#4590),#5011,.T.);
#5228=ADVANCED_FACE('',(#4591),#704,.F.);
#5229=ADVANCED_FACE('',(#4592),#705,.F.);
#5230=ADVANCED_FACE('',(#4593,#4594),#10,.T.);
#5231=ADVANCED_FACE('',(#4595,#4596),#706,.F.);
#5232=ADVANCED_FACE('',(#4597,#4598),#18,.F.);
#5233=ADVANCED_FACE('',(#4599),#19,.T.);
#5234=ADVANCED_FACE('',(#4600),#707,.T.);
#5235=ADVANCED_FACE('',(#4601),#708,.F.);
#5236=ADVANCED_FACE('',(#4602),#709,.T.);
#5237=ADVANCED_FACE('',(#4603,#4604),#11,.T.);
#5540=CLOSED_SHELL('',(#5225,#5226,#5227,#5228,#5229,#5230,#5231,#5232,
#5233,#5234,#5235,#5236,#5237));
#5554=STYLED_ITEM('',(#5568),#5659);
#5568=PRESENTATION_STYLE_ASSIGNMENT((#5582));
#5582=SURFACE_STYLE_USAGE(.BOTH.,#5596);
#5596=SURFACE_SIDE_STYLE('',(#5610));
#5610=SURFACE_STYLE_FILL_AREA(#5624);
#5624=FILL_AREA_STYLE('',(#5638));
#5638=FILL_AREA_STYLE_COLOUR('',#5652);
#5652=COLOUR_RGB('', 0.31764706, 0.68627451, 0.89019608);
#5659=MANIFOLD_SOLID_BREP('Slotted cheese head screw M2.5x0.45 x 10',#5540);
#5674=SHAPE_DEFINITION_REPRESENTATION(#10180,#5690);
#5690=SHAPE_REPRESENTATION('Slotted cheese head screw M2.5x0.45 x 10',(#5704),
#10144);
#5704=AXIS2_PLACEMENT_3D('',#8391,#6505,#6506);
#5732=AXIS2_PLACEMENT_3D('',#8457,#6561,#6562);
#5733=AXIS2_PLACEMENT_3D('',#8461,#6564,#6565);
#5734=AXIS2_PLACEMENT_3D('',#8462,#6566,#6567);
#5735=AXIS2_PLACEMENT_3D('',#8463,#6568,#6569);
#5736=AXIS2_PLACEMENT_3D('',#8471,#6570,#6571);
#5737=AXIS2_PLACEMENT_3D('',#8477,#6572,#6573);
#5738=AXIS2_PLACEMENT_3D('',#8478,#6574,#6575);
#5739=AXIS2_PLACEMENT_3D('',#8480,#6576,#6577);
#5740=AXIS2_PLACEMENT_3D('',#8482,#6578,#6579);
#5741=AXIS2_PLACEMENT_3D('',#8483,#6580,#6581);
#5742=AXIS2_PLACEMENT_3D('',#8485,#6582,#6583);
#5743=AXIS2_PLACEMENT_3D('',#8487,#6585,#6586);
#5744=AXIS2_PLACEMENT_3D('',#8488,#6587,#6588);
#5745=AXIS2_PLACEMENT_3D('',#8496,#6589,#6590);
#5746=AXIS2_PLACEMENT_3D('',#8507,#6591,#6592);
#5747=AXIS2_PLACEMENT_3D('',#8513,#6593,#6594);
#5748=AXIS2_PLACEMENT_3D('',#8515,#6595,#6596);
#5749=AXIS2_PLACEMENT_3D('',#8516,#6597,#6598);
#5750=AXIS2_PLACEMENT_3D('',#8518,#6599,#6600);
#5751=AXIS2_PLACEMENT_3D('',#8519,#6601,#6602);
#5752=AXIS2_PLACEMENT_3D('',#8528,#6603,#6604);
#5753=AXIS2_PLACEMENT_3D('',#8531,#6607,#6608);
#5754=AXIS2_PLACEMENT_3D('',#8532,#6609,#6610);
#5755=AXIS2_PLACEMENT_3D('',#8533,#6611,#6612);
#6505=DIRECTION('',(0.,0.,1.));
#6506=DIRECTION('',(1.,0.,0.));
#6561=DIRECTION('',(0.,0.,-1.));
#6562=DIRECTION('',(-1.,0.,0.));
#6563=DIRECTION('',(1.,0.,0.));
#6564=DIRECTION('',(0.,0.,-1.));
#6565=DIRECTION('',(-1.,0.,0.));
#6566=DIRECTION('',(0.,0.,-1.));
#6567=DIRECTION('',(-1.,0.,0.));
#6568=DIRECTION('',(0.,0.,1.));
#6569=DIRECTION('',(1.,0.,0.));
#6570=DIRECTION('',(0.,0.,-1.));
#6571=DIRECTION('',(-1.,0.,0.));
#6572=DIRECTION('',(0.,0.,-1.));
#6573=DIRECTION('',(-1.,0.,0.));
#6574=DIRECTION('',(0.,0.,1.));
#6575=DIRECTION('',(1.,0.,0.));
#6576=DIRECTION('',(0.,0.,-1.));
#6577=DIRECTION('',(-1.,0.,0.));
#6578=DIRECTION('',(0.,0.,1.));
#6579=DIRECTION('',(1.,0.,0.));
#6580=DIRECTION('',(0.,0.,1.));
#6581=DIRECTION('',(1.,0.,0.));
#6582=DIRECTION('',(0.,0.,-1.));
#6583=DIRECTION('',(-1.,0.,0.));
#6584=DIRECTION('',(1.,0.,0.));
#6585=DIRECTION('',(0.,0.,-1.));
#6586=DIRECTION('',(-1.,0.,0.));
#6587=DIRECTION('',(0.,0.,1.));
#6588=DIRECTION('',(1.,0.,0.));
#6589=DIRECTION('',(0.,0.,1.));
#6590=DIRECTION('',(1.,0.,0.));
#6591=DIRECTION('',(0.,0.,1.));
#6592=DIRECTION('',(1.,0.,0.));
#6593=DIRECTION('',(0.,0.,-1.));
#6594=DIRECTION('',(-1.,0.,0.));
#6595=DIRECTION('',(0.,0.,1.));
#6596=DIRECTION('',(1.,0.,0.));
#6597=DIRECTION('',(0.,0.,-1.));
#6598=DIRECTION('',(-1.,0.,0.));
#6599=DIRECTION('',(0.,0.,-1.));
#6600=DIRECTION('',(-1.,0.,0.));
#6601=DIRECTION('',(0.,0.,-1.));
#6602=DIRECTION('',(-1.,0.,0.));
#6603=DIRECTION('',(0.,0.,1.));
#6604=DIRECTION('',(1.,0.,0.));
#6605=DIRECTION('',(1.,0.,0.));
#6606=DIRECTION('',(1.,0.,0.));
#6607=DIRECTION('',(0.,-1.,0.));
#6608=DIRECTION('',(0.,0.,-1.));
#6609=DIRECTION('',(0.,-1.,0.));
#6610=DIRECTION('',(0.,0.,-1.));
#6611=DIRECTION('',(0.,0.,1.));
#6612=DIRECTION('',(1.,0.,0.));
#8391=CARTESIAN_POINT('',(0.,0.,0.));
#8457=CARTESIAN_POINT('',(-0.00104626020282667,0.,6.50521303491303E-19));
#8458=CARTESIAN_POINT('',(0.,-0.0003,6.50521303491303E-19));
#8459=CARTESIAN_POINT('',(-0.00197826943066075,-0.0003,6.50521303491303E-19));
#8460=CARTESIAN_POINT('',(0.00197826943066075,-0.0003,6.50521303491303E-19));
#8461=CARTESIAN_POINT('',(0.,0.,6.50521303491303E-19));
#8462=CARTESIAN_POINT('',(0.,0.,-0.0001));
#8463=CARTESIAN_POINT('',(0.,0.,-9.12844257252368E-5));
#8464=CARTESIAN_POINT('',(-0.00207897297737586,0.0003,-9.12844257252367E-5));
#8465=CARTESIAN_POINT('',(0.00207897297737584,0.0003,-9.12844257252368E-5));
#8466=CARTESIAN_POINT('',(-0.00207897297737584,0.0003,-9.12844257252392E-5));
#8467=CARTESIAN_POINT('',(-0.00207459712624839,0.0003,-4.17809699915527E-5));
#8468=CARTESIAN_POINT('',(-0.00202837661239549,0.0003,-6.48859435981983E-19));
#8469=CARTESIAN_POINT('',(-0.00197826943066076,0.0003,3.05634754505891E-21));
#8470=CARTESIAN_POINT('',(-0.00197826943066075,0.0003,6.50521303491303E-19));
#8471=CARTESIAN_POINT('',(0.,0.,6.50521303491303E-19));
#8472=CARTESIAN_POINT('',(0.00197826943066075,0.0003,6.50521303491303E-19));
#8473=CARTESIAN_POINT('',(0.00197826943066076,0.0003,1.75840007344507E-18));
#8474=CARTESIAN_POINT('',(0.00202795255984864,0.0003,1.11200139422846E-18));
#8475=CARTESIAN_POINT('',(0.00207460838288334,0.0003,-4.19083148928644E-5));
#8476=CARTESIAN_POINT('',(0.00207897297737584,0.0003,-9.12844257252363E-5));
#8477=CARTESIAN_POINT('',(0.,0.,-0.0059));
#8478=CARTESIAN_POINT('',(0.,0.,-0.01155643035625));
#8479=CARTESIAN_POINT('',(0.00125,0.,-0.01155643035625));
#8480=CARTESIAN_POINT('',(0.,0.,-0.0019));
#8481=CARTESIAN_POINT('',(-0.00125,0.,-0.0019));
#8482=CARTESIAN_POINT('',(-0.000625,0.,-0.0118));
#8483=CARTESIAN_POINT('',(0.,0.,-0.0118));
#8484=CARTESIAN_POINT('',(0.00100643035625,0.,-0.0118));
#8485=CARTESIAN_POINT('',(-0.00104626020282667,0.,6.50521303491303E-19));
#8486=CARTESIAN_POINT('',(-5.01008275896316E-5,0.0003,6.50521303491303E-19));
#8487=CARTESIAN_POINT('',(0.,0.,1.7347234759768E-18));
#8488=CARTESIAN_POINT('',(0.,0.,-9.12844257252368E-5));
#8489=CARTESIAN_POINT('',(0.00207897297737919,-0.0003,-9.12844257253807E-5));
#8490=CARTESIAN_POINT('',(-0.00207897297737586,-0.0003,-9.12844257252367E-5));
#8491=CARTESIAN_POINT('',(-0.00207897297737588,-0.0003,-9.12844257252345E-5));
#8492=CARTESIAN_POINT('',(-0.00209690871796292,-0.0003,-0.000294189212551693));
#8493=CARTESIAN_POINT('',(-0.00211483976375729,-0.0003,-0.000497094414503251));
#8494=CARTESIAN_POINT('',(-0.00213276646112605,-0.0003,-0.000699999999999993));
#8495=CARTESIAN_POINT('',(-0.00213276646112597,-0.0003,-0.0007));
#8496=CARTESIAN_POINT('',(0.,0.,-0.0007));
#8497=CARTESIAN_POINT('',(-0.00213276646112597,0.0003,-0.0007));
#8498=CARTESIAN_POINT('',(-0.00207897297737588,0.0003,-9.12844257252349E-5));
#8499=CARTESIAN_POINT('',(-0.00209690871796292,0.0003,-0.000294189212551693));
#8500=CARTESIAN_POINT('',(-0.00211483976375729,0.0003,-0.000497094414503251));
#8501=CARTESIAN_POINT('',(-0.00213276646112605,0.0003,-0.000699999999999993));
#8502=CARTESIAN_POINT('',(0.00213276646112605,0.0003,-0.000699999999999993));
#8503=CARTESIAN_POINT('',(0.00211483976374573,0.0003,-0.000497094414372398));
#8504=CARTESIAN_POINT('',(0.00209690871792154,0.0003,-0.000294189212083583));
#8505=CARTESIAN_POINT('',(0.00207897297737588,0.0003,-9.12844257252331E-5));
#8506=CARTESIAN_POINT('',(0.00213276646112597,0.0003,-0.0007));
#8507=CARTESIAN_POINT('',(0.,0.,-0.0007));
#8508=CARTESIAN_POINT('',(0.00213276646112597,-0.0003,-0.0007));
#8509=CARTESIAN_POINT('',(0.00213276646112605,-0.0003,-0.000699999999999993));
#8510=CARTESIAN_POINT('',(0.00211483976374574,-0.0003,-0.000497094414372544));
#8511=CARTESIAN_POINT('',(0.00209690871792157,-0.0003,-0.000294189212083876));
#8512=CARTESIAN_POINT('',(0.00207897297737592,-0.0003,-9.12844257256711E-5));
#8513=CARTESIAN_POINT('',(0.,0.,-0.0018));
#8514=CARTESIAN_POINT('',(-0.00225,0.,-0.0018));
#8515=CARTESIAN_POINT('',(-0.0018,0.,-0.0018));
#8516=CARTESIAN_POINT('',(0.,0.,-0.0018));
#8517=CARTESIAN_POINT('',(-0.00135,0.,-0.0018));
#8518=CARTESIAN_POINT('',(0.,0.,-0.0019));
#8519=CARTESIAN_POINT('',(0.,0.,-0.0001));
#8520=CARTESIAN_POINT('',(-0.00207897297737584,-0.0003,-9.12844257252392E-5));
#8521=CARTESIAN_POINT('',(-0.00207459712624839,-0.0003,-4.17809699915526E-5));
#8522=CARTESIAN_POINT('',(-0.00202837661239549,-0.0003,-6.54219152761022E-19));
#8523=CARTESIAN_POINT('',(-0.00197826943066076,-0.0003,-2.30336923397844E-21));
#8524=CARTESIAN_POINT('',(0.00197826943066075,-0.0003,1.76771743586486E-18));
#8525=CARTESIAN_POINT('',(0.00202795255984883,-0.0003,1.12131875664574E-18));
#8526=CARTESIAN_POINT('',(0.00207460838288366,-0.0003,-4.19083148932107E-5));
#8527=CARTESIAN_POINT('',(0.00207897297737589,-0.0003,-9.12844257258122E-5));
#8528=CARTESIAN_POINT('',(0.,0.,-0.0007));
#8529=CARTESIAN_POINT('',(0.,-0.0003,-0.0007));
#8530=CARTESIAN_POINT('',(-5.01008275896316E-5,0.0003,-0.0007));
#8531=CARTESIAN_POINT('',(0.,-0.0003,-0.0007));
#8532=CARTESIAN_POINT('',(-5.01008275896316E-5,0.0003,-0.0007));
#8533=CARTESIAN_POINT('',(0.,0.,-0.0118));
#10141=MECHANICAL_DESIGN_GEOMETRIC_PRESENTATION_REPRESENTATION('',(#5554),#10142);
#10142=(
GEOMETRIC_REPRESENTATION_CONTEXT(3)
GLOBAL_UNCERTAINTY_ASSIGNED_CONTEXT((#10158))
GLOBAL_UNIT_ASSIGNED_CONTEXT((#10176,#10175,#10174))
REPRESENTATION_CONTEXT('MAS-674','TOP_LEVEL_ASSEMBLY_PART')
);
#10144=(
GEOMETRIC_REPRESENTATION_CONTEXT(3)
GLOBAL_UNCERTAINTY_ASSIGNED_CONTEXT((#10160))
GLOBAL_UNIT_ASSIGNED_CONTEXT((#10176,#10175,#10174))
REPRESENTATION_CONTEXT('Slotted cheese head screw M2.5x0.45 x 10',
'COMPONENT_PART')
);
#10158=UNCERTAINTY_MEASURE_WITH_UNIT(LENGTH_MEASURE(1.E-8),#10176,
'DISTANCE_ACCURACY_VALUE','Maximum Tolerance applied to model');
#10160=UNCERTAINTY_MEASURE_WITH_UNIT(LENGTH_MEASURE(2.E-5),#10176,
'DISTANCE_ACCURACY_VALUE','Maximum Tolerance applied to model');
#10174=(
NAMED_UNIT(*)
SI_UNIT($,.STERADIAN.)
SOLID_ANGLE_UNIT()
);
#10175=(
NAMED_UNIT(*)
PLANE_ANGLE_UNIT()
SI_UNIT($,.RADIAN.)
);
#10176=(
LENGTH_UNIT()
NAMED_UNIT(*)
SI_UNIT($,.METRE.)
);
#10180=PRODUCT_DEFINITION_SHAPE('','',#10212);
#10212=PRODUCT_DEFINITION('','',#10244,#10228);
#10228=PRODUCT_DEFINITION_CONTEXT('',#10323,'design');
#10244=PRODUCT_DEFINITION_FORMATION_WITH_SPECIFIED_SOURCE('','',#10276,
 .NOT_KNOWN.);
#10276=PRODUCT('Slotted cheese head screw M2.5x0.45 x 10',
'Slotted cheese head screw M2.5x0.45 x 10',
'Slotted cheese head screw M2.5x0.45 x 10',(#10308));
#10308=PRODUCT_CONTEXT('',#10323,'mechanical');
#10323=APPLICATION_CONTEXT('managed model based 3d engineering');
ENDSEC;
END-ISO-10303-21;
